ISO-10303-21;
HEADER;
/* Generated by software containing ST-Developer
 * from STEP Tools, Inc. (www.steptools.com) 
 */

FILE_DESCRIPTION(
/* description */ ('PAT-015'),
/* implementation_level */ '2;1');

FILE_NAME(
/* name */ 'O-Ring.step',
/* time_stamp */ '2026-10-29T16:03:43-07:00',
/* author */ (''),
/* organization */ (''),
/* preprocessor_version */ 'ST-DEVELOPER v20.2',
/* originating_system */ 'Autodesk Translation Framework v15.17.0.0',
/* authorisation */ '');

FILE_SCHEMA (('AUTOMOTIVE_DESIGN { 1 0 10303 214 3 1 1 }'));
ENDSEC;

DATA;
#10=MECHANICAL_DESIGN_GEOMETRIC_PRESENTATION_REPRESENTATION('',(#252),#10266);
#183=TOROIDAL_SURFACE('',#5482,0.7495,0.131);
#204=SHAPE_REPRESENTATION_RELATIONSHIP('SRR','None',#10375,#227);
#227=ADVANCED_BREP_SHAPE_REPRESENTATION('',(#276),#10263);
#252=STYLED_ITEM('',(#10554),#276);
#276=MANIFOLD_SOLID_BREP('Body1',#4712);
#829=FACE_OUTER_BOUND('',#1237,.T.);
#1237=EDGE_LOOP('',(#4193,#4194,#4195,#4196));
#2102=CIRCLE('',#5483,0.131);
#2103=CIRCLE('',#5484,0.6185);
#2475=VERTEX_POINT('',#10076);
#3052=EDGE_CURVE('',#2475,#2475,#2102,.T.);
#3053=EDGE_CURVE('',#2475,#2475,#2103,.T.);
#4193=ORIENTED_EDGE('',*,*,#3052,.F.);
#4194=ORIENTED_EDGE('',*,*,#3053,.T.);
#4195=ORIENTED_EDGE('',*,*,#3052,.T.);
#4196=ORIENTED_EDGE('',*,*,#3053,.F.);
#4664=ADVANCED_FACE('',(#829),#183,.T.);
#4712=CLOSED_SHELL('',(#4664));
#5481=AXIS2_PLACEMENT_3D('',#10074,#6821,#6822);
#5482=AXIS2_PLACEMENT_3D('',#10075,#6823,#6824);
#5483=AXIS2_PLACEMENT_3D('',#10077,#6825,#6826);
#5484=AXIS2_PLACEMENT_3D('',#10078,#6827,#6828);
#6821=DIRECTION('axis',(0.,0.,1.));
#6822=DIRECTION('refdir',(1.,0.,0.));
#6823=DIRECTION('center_axis',(0.,-1.,0.));
#6824=DIRECTION('ref_axis',(0.,0.,-1.));
#6825=DIRECTION('center_axis',(-1.,0.,-1.22464679914735E-16));
#6826=DIRECTION('ref_axis',(-1.22464679914735E-16,0.,1.));
#6827=DIRECTION('center_axis',(0.,1.,0.));
#6828=DIRECTION('ref_axis',(0.,0.,-1.));
#10074=CARTESIAN_POINT('',(0.,0.,0.));
#10075=CARTESIAN_POINT('Origin',(0.,0.,0.));
#10076=CARTESIAN_POINT('',(-7.57444045272638E-17,-1.60428730688303E-17,
0.6185));
#10077=CARTESIAN_POINT('Origin',(-9.17872775960941E-17,0.,0.7495));
#10078=CARTESIAN_POINT('Origin',(0.,1.60428730688303E-17,0.));
#10238=UNCERTAINTY_MEASURE_WITH_UNIT(LENGTH_MEASURE(0.001),#10267,
'DISTANCE_ACCURACY_VALUE',
'Maximum model space distance between geometric entities at asserted c
onnectivities');
#10241=UNCERTAINTY_MEASURE_WITH_UNIT(LENGTH_MEASURE(0.001),#10267,
'DISTANCE_ACCURACY_VALUE',
'Maximum model space distance between geometric entities at asserted c
onnectivities');
#10263=(
GEOMETRIC_REPRESENTATION_CONTEXT(3)
GLOBAL_UNCERTAINTY_ASSIGNED_CONTEXT((#10238))
GLOBAL_UNIT_ASSIGNED_CONTEXT((#10267,#10269,#10270))
REPRESENTATION_CONTEXT('','3D')
);
#10266=(
GEOMETRIC_REPRESENTATION_CONTEXT(3)
GLOBAL_UNCERTAINTY_ASSIGNED_CONTEXT((#10241))
GLOBAL_UNIT_ASSIGNED_CONTEXT((#10267,#10269,#10270))
REPRESENTATION_CONTEXT('','3D')
);
#10267=(
LENGTH_UNIT()
NAMED_UNIT(*)
SI_UNIT(.CENTI.,.METRE.)
);
#10269=(
NAMED_UNIT(*)
PLANE_ANGLE_UNIT()
SI_UNIT($,.RADIAN.)
);
#10270=(
NAMED_UNIT(*)
SI_UNIT($,.STERADIAN.)
SOLID_ANGLE_UNIT()
);
#10292=SHAPE_DEFINITION_REPRESENTATION(#10316,#10375);
#10316=PRODUCT_DEFINITION_SHAPE('',$,#10400);
#10375=SHAPE_REPRESENTATION('',(#5481),#10263);
#10378=PRODUCT_DEFINITION_CONTEXT('part definition',#10452,'design');
#10400=PRODUCT_DEFINITION('O-Ring','O-Ring',#10424,#10378);
#10424=PRODUCT_DEFINITION_FORMATION('',$,#10475);
#10452=APPLICATION_CONTEXT(
'Core Data for Automotive Mechanical Design Process');
#10453=PRODUCT_CONTEXT('part definition',#10452,'mechanical');
#10475=PRODUCT('O-Ring','O-Ring','O-Ring',(#10453));
#10548=COLOUR_RGB('Black',0.12,0.14,0.17);
#10549=FILL_AREA_STYLE_COLOUR('',#10548);
#10550=FILL_AREA_STYLE('',(#10549));
#10551=SURFACE_STYLE_FILL_AREA(#10550);
#10552=SURFACE_SIDE_STYLE('',(#10551));
#10553=SURFACE_STYLE_USAGE(.BOTH.,#10552);
#10554=PRESENTATION_STYLE_ASSIGNMENT((#10553));
ENDSEC;
END-ISO-10303-21;
